ISO-10303-21;
HEADER;
/* Generated by software containing ST-Developer
 * from STEP Tools, Inc. (www.steptools.com) 
 */

FILE_DESCRIPTION(
/* description */ ('Horizontal push-pull toggle clamp'),
/* implementation_level */ '2;1');

FILE_NAME(
/* name */ 'M5x14 Cap Screw.step',
/* time_stamp */ '2026-10-27T21:21:09-07:00',
/* author */ (''),
/* organization */ (''),
/* preprocessor_version */ 'ST-DEVELOPER v20.2',
/* originating_system */ 'Autodesk Translation Framework v15.17.0.0',
/* authorisation */ '');

FILE_SCHEMA (('AUTOMOTIVE_DESIGN { 1 0 10303 214 3 1 1 }'));
ENDSEC;

DATA;
#10=MECHANICAL_DESIGN_GEOMETRIC_PRESENTATION_REPRESENTATION('',(#188),#4791);
#148=CONICAL_SURFACE('',#2904,0.4,0.785398163397448);
#149=CONICAL_SURFACE('',#2908,0.41,0.785398163397448);
#150=CONICAL_SURFACE('',#2912,0.26,0.463647609000806);
#157=ORIENTED_CLOSED_SHELL('',*,#2632,.F.);
#158=BREP_WITH_VOIDS('Body1',#2633,(#157));
#162=SHAPE_REPRESENTATION_RELATIONSHIP('SRR','None',#4866,#175);
#175=ADVANCED_BREP_SHAPE_REPRESENTATION('',(#158),#4779);
#188=STYLED_ITEM('',(#5030),#158);
#235=FACE_BOUND('',#616,.T.);
#306=PLANE('',#2892);
#307=PLANE('',#2893);
#308=PLANE('',#2894);
#309=PLANE('',#2895);
#310=PLANE('',#2896);
#311=PLANE('',#2897);
#312=PLANE('',#2898);
#313=PLANE('',#2899);
#314=PLANE('',#2900);
#315=PLANE('',#2902);
#316=PLANE('',#2910);
#426=FACE_OUTER_BOUND('',#602,.T.);
#427=FACE_OUTER_BOUND('',#603,.T.);
#428=FACE_OUTER_BOUND('',#604,.T.);
#429=FACE_OUTER_BOUND('',#605,.T.);
#430=FACE_OUTER_BOUND('',#606,.T.);
#431=FACE_OUTER_BOUND('',#607,.T.);
#432=FACE_OUTER_BOUND('',#608,.T.);
#433=FACE_OUTER_BOUND('',#609,.T.);
#434=FACE_OUTER_BOUND('',#610,.T.);
#435=FACE_OUTER_BOUND('',#611,.T.);
#436=FACE_OUTER_BOUND('',#612,.T.);
#437=FACE_OUTER_BOUND('',#613,.T.);
#438=FACE_OUTER_BOUND('',#614,.T.);
#439=FACE_OUTER_BOUND('',#615,.T.);
#440=FACE_OUTER_BOUND('',#617,.T.);
#441=FACE_OUTER_BOUND('',#618,.T.);
#602=EDGE_LOOP('',(#2089,#2090,#2091,#2092));
#603=EDGE_LOOP('',(#2093,#2094,#2095,#2096));
#604=EDGE_LOOP('',(#2097,#2098,#2099,#2100));
#605=EDGE_LOOP('',(#2101,#2102,#2103,#2104));
#606=EDGE_LOOP('',(#2105,#2106,#2107,#2108));
#607=EDGE_LOOP('',(#2109,#2110,#2111,#2112));
#608=EDGE_LOOP('',(#2113,#2114,#2115,#2116,#2117,#2118));
#609=EDGE_LOOP('',(#2119,#2120,#2121,#2122,#2123,#2124));
#610=EDGE_LOOP('',(#2125));
#611=EDGE_LOOP('',(#2126));
#612=EDGE_LOOP('',(#2127,#2128,#2129,#2130));
#613=EDGE_LOOP('',(#2131,#2132,#2133,#2134));
#614=EDGE_LOOP('',(#2135,#2136,#2137,#2138));
#615=EDGE_LOOP('',(#2139));
#616=EDGE_LOOP('',(#2140));
#617=EDGE_LOOP('',(#2141,#2142,#2143,#2144));
#618=EDGE_LOOP('',(#2145,#2146,#2147,#2148));
#744=CIRCLE('',#2901,0.24505);
#745=CIRCLE('',#2903,0.375);
#746=CIRCLE('',#2905,0.425);
#747=CIRCLE('',#2907,0.425);
#748=CIRCLE('',#2909,0.395);
#749=CIRCLE('',#2911,0.27);
#750=CIRCLE('',#2913,0.24505);
#915=LINE('',#4185,#1135);
#916=LINE('',#4187,#1136);
#917=LINE('',#4189,#1137);
#918=LINE('',#4190,#1138);
#919=LINE('',#4193,#1139);
#920=LINE('',#4195,#1140);
#921=LINE('',#4196,#1141);
#922=LINE('',#4199,#1142);
#923=LINE('',#4201,#1143);
#924=LINE('',#4202,#1144);
#925=LINE('',#4205,#1145);
#926=LINE('',#4207,#1146);
#927=LINE('',#4208,#1147);
#928=LINE('',#4211,#1148);
#929=LINE('',#4213,#1149);
#930=LINE('',#4214,#1150);
#931=LINE('',#4216,#1151);
#932=LINE('',#4217,#1152);
#933=LINE('',#4229,#1153);
#934=LINE('',#4233,#1154);
#935=LINE('',#4237,#1155);
#936=LINE('',#4244,#1156);
#937=LINE('',#4246,#1157);
#1135=VECTOR('',#3401,1.);
#1136=VECTOR('',#3402,1.);
#1137=VECTOR('',#3403,1.);
#1138=VECTOR('',#3404,1.);
#1139=VECTOR('',#3407,1.);
#1140=VECTOR('',#3408,1.);
#1141=VECTOR('',#3409,1.);
#1142=VECTOR('',#3412,1.);
#1143=VECTOR('',#3413,1.);
#1144=VECTOR('',#3414,1.);
#1145=VECTOR('',#3417,1.);
#1146=VECTOR('',#3418,1.);
#1147=VECTOR('',#3419,1.);
#1148=VECTOR('',#3422,1.);
#1149=VECTOR('',#3423,1.);
#1150=VECTOR('',#3424,1.);
#1151=VECTOR('',#3427,1.);
#1152=VECTOR('',#3428,1.);
#1153=VECTOR('',#3445,0.4);
#1154=VECTOR('',#3450,0.425);
#1155=VECTOR('',#3455,0.41);
#1156=VECTOR('',#3464,0.26);
#1157=VECTOR('',#3467,0.25);
#1338=VERTEX_POINT('',#4183);
#1339=VERTEX_POINT('',#4184);
#1340=VERTEX_POINT('',#4186);
#1341=VERTEX_POINT('',#4188);
#1342=VERTEX_POINT('',#4192);
#1343=VERTEX_POINT('',#4194);
#1344=VERTEX_POINT('',#4198);
#1345=VERTEX_POINT('',#4200);
#1346=VERTEX_POINT('',#4204);
#1347=VERTEX_POINT('',#4206);
#1348=VERTEX_POINT('',#4210);
#1349=VERTEX_POINT('',#4212);
#1350=VERTEX_POINT('',#4221);
#1351=VERTEX_POINT('',#4224);
#1352=VERTEX_POINT('',#4227);
#1353=VERTEX_POINT('',#4231);
#1354=VERTEX_POINT('',#4235);
#1355=VERTEX_POINT('',#4239);
#1356=VERTEX_POINT('',#4242);
#1606=EDGE_CURVE('',#1338,#1339,#915,.T.);
#1607=EDGE_CURVE('',#1339,#1340,#916,.T.);
#1608=EDGE_CURVE('',#1340,#1341,#917,.T.);
#1609=EDGE_CURVE('',#1338,#1341,#918,.T.);
#1610=EDGE_CURVE('',#1339,#1342,#919,.T.);
#1611=EDGE_CURVE('',#1342,#1343,#920,.T.);
#1612=EDGE_CURVE('',#1343,#1340,#921,.T.);
#1613=EDGE_CURVE('',#1342,#1344,#922,.T.);
#1614=EDGE_CURVE('',#1344,#1345,#923,.T.);
#1615=EDGE_CURVE('',#1345,#1343,#924,.T.);
#1616=EDGE_CURVE('',#1344,#1346,#925,.T.);
#1617=EDGE_CURVE('',#1346,#1347,#926,.T.);
#1618=EDGE_CURVE('',#1347,#1345,#927,.T.);
#1619=EDGE_CURVE('',#1346,#1348,#928,.T.);
#1620=EDGE_CURVE('',#1348,#1349,#929,.T.);
#1621=EDGE_CURVE('',#1349,#1347,#930,.T.);
#1622=EDGE_CURVE('',#1348,#1338,#931,.T.);
#1623=EDGE_CURVE('',#1341,#1349,#932,.T.);
#1624=EDGE_CURVE('',#1350,#1350,#744,.T.);
#1625=EDGE_CURVE('',#1351,#1351,#745,.T.);
#1626=EDGE_CURVE('',#1352,#1352,#746,.T.);
#1627=EDGE_CURVE('',#1352,#1351,#933,.T.);
#1628=EDGE_CURVE('',#1353,#1353,#747,.T.);
#1629=EDGE_CURVE('',#1353,#1352,#934,.T.);
#1630=EDGE_CURVE('',#1354,#1354,#748,.T.);
#1631=EDGE_CURVE('',#1354,#1353,#935,.T.);
#1632=EDGE_CURVE('',#1355,#1355,#749,.T.);
#1633=EDGE_CURVE('',#1356,#1356,#750,.F.);
#1634=EDGE_CURVE('',#1356,#1355,#936,.T.);
#1635=EDGE_CURVE('',#1350,#1356,#937,.T.);
#2089=ORIENTED_EDGE('',*,*,#1606,.T.);
#2090=ORIENTED_EDGE('',*,*,#1607,.T.);
#2091=ORIENTED_EDGE('',*,*,#1608,.T.);
#2092=ORIENTED_EDGE('',*,*,#1609,.F.);
#2093=ORIENTED_EDGE('',*,*,#1610,.T.);
#2094=ORIENTED_EDGE('',*,*,#1611,.T.);
#2095=ORIENTED_EDGE('',*,*,#1612,.T.);
#2096=ORIENTED_EDGE('',*,*,#1607,.F.);
#2097=ORIENTED_EDGE('',*,*,#1613,.T.);
#2098=ORIENTED_EDGE('',*,*,#1614,.T.);
#2099=ORIENTED_EDGE('',*,*,#1615,.T.);
#2100=ORIENTED_EDGE('',*,*,#1611,.F.);
#2101=ORIENTED_EDGE('',*,*,#1616,.T.);
#2102=ORIENTED_EDGE('',*,*,#1617,.T.);
#2103=ORIENTED_EDGE('',*,*,#1618,.T.);
#2104=ORIENTED_EDGE('',*,*,#1614,.F.);
#2105=ORIENTED_EDGE('',*,*,#1619,.T.);
#2106=ORIENTED_EDGE('',*,*,#1620,.T.);
#2107=ORIENTED_EDGE('',*,*,#1621,.T.);
#2108=ORIENTED_EDGE('',*,*,#1617,.F.);
#2109=ORIENTED_EDGE('',*,*,#1622,.T.);
#2110=ORIENTED_EDGE('',*,*,#1609,.T.);
#2111=ORIENTED_EDGE('',*,*,#1623,.T.);
#2112=ORIENTED_EDGE('',*,*,#1620,.F.);
#2113=ORIENTED_EDGE('',*,*,#1622,.F.);
#2114=ORIENTED_EDGE('',*,*,#1619,.F.);
#2115=ORIENTED_EDGE('',*,*,#1616,.F.);
#2116=ORIENTED_EDGE('',*,*,#1613,.F.);
#2117=ORIENTED_EDGE('',*,*,#1610,.F.);
#2118=ORIENTED_EDGE('',*,*,#1606,.F.);
#2119=ORIENTED_EDGE('',*,*,#1623,.F.);
#2120=ORIENTED_EDGE('',*,*,#1608,.F.);
#2121=ORIENTED_EDGE('',*,*,#1612,.F.);
#2122=ORIENTED_EDGE('',*,*,#1615,.F.);
#2123=ORIENTED_EDGE('',*,*,#1618,.F.);
#2124=ORIENTED_EDGE('',*,*,#1621,.F.);
#2125=ORIENTED_EDGE('',*,*,#1624,.F.);
#2126=ORIENTED_EDGE('',*,*,#1625,.F.);
#2127=ORIENTED_EDGE('',*,*,#1626,.F.);
#2128=ORIENTED_EDGE('',*,*,#1627,.T.);
#2129=ORIENTED_EDGE('',*,*,#1625,.T.);
#2130=ORIENTED_EDGE('',*,*,#1627,.F.);
#2131=ORIENTED_EDGE('',*,*,#1628,.F.);
#2132=ORIENTED_EDGE('',*,*,#1629,.T.);
#2133=ORIENTED_EDGE('',*,*,#1626,.T.);
#2134=ORIENTED_EDGE('',*,*,#1629,.F.);
#2135=ORIENTED_EDGE('',*,*,#1630,.F.);
#2136=ORIENTED_EDGE('',*,*,#1631,.T.);
#2137=ORIENTED_EDGE('',*,*,#1628,.T.);
#2138=ORIENTED_EDGE('',*,*,#1631,.F.);
#2139=ORIENTED_EDGE('',*,*,#1630,.T.);
#2140=ORIENTED_EDGE('',*,*,#1632,.F.);
#2141=ORIENTED_EDGE('',*,*,#1633,.F.);
#2142=ORIENTED_EDGE('',*,*,#1634,.T.);
#2143=ORIENTED_EDGE('',*,*,#1632,.T.);
#2144=ORIENTED_EDGE('',*,*,#1634,.F.);
#2145=ORIENTED_EDGE('',*,*,#1624,.T.);
#2146=ORIENTED_EDGE('',*,*,#1635,.T.);
#2147=ORIENTED_EDGE('',*,*,#1633,.T.);
#2148=ORIENTED_EDGE('',*,*,#1635,.F.);
#2457=CYLINDRICAL_SURFACE('',#2906,0.425);
#2458=CYLINDRICAL_SURFACE('',#2914,0.24505);
#2542=ADVANCED_FACE('',(#426),#306,.F.);
#2543=ADVANCED_FACE('',(#427),#307,.F.);
#2544=ADVANCED_FACE('',(#428),#308,.F.);
#2545=ADVANCED_FACE('',(#429),#309,.F.);
#2546=ADVANCED_FACE('',(#430),#310,.F.);
#2547=ADVANCED_FACE('',(#431),#311,.F.);
#2548=ADVANCED_FACE('',(#432),#312,.F.);
#2549=ADVANCED_FACE('',(#433),#313,.F.);
#2550=ADVANCED_FACE('',(#434),#314,.F.);
#2551=ADVANCED_FACE('',(#435),#315,.T.);
#2552=ADVANCED_FACE('',(#436),#148,.T.);
#2553=ADVANCED_FACE('',(#437),#2457,.T.);
#2554=ADVANCED_FACE('',(#438),#149,.T.);
#2555=ADVANCED_FACE('',(#439,#235),#316,.T.);
#2556=ADVANCED_FACE('',(#440),#150,.T.);
#2557=ADVANCED_FACE('',(#441),#2458,.T.);
#2632=CLOSED_SHELL('',(#2542,#2543,#2544,#2545,#2546,#2547,#2548,#2549));
#2633=CLOSED_SHELL('',(#2550,#2551,#2552,#2553,#2554,#2555,#2556,#2557));
#2891=AXIS2_PLACEMENT_3D('',#4181,#3397,#3398);
#2892=AXIS2_PLACEMENT_3D('',#4182,#3399,#3400);
#2893=AXIS2_PLACEMENT_3D('',#4191,#3405,#3406);
#2894=AXIS2_PLACEMENT_3D('',#4197,#3410,#3411);
#2895=AXIS2_PLACEMENT_3D('',#4203,#3415,#3416);
#2896=AXIS2_PLACEMENT_3D('',#4209,#3420,#3421);
#2897=AXIS2_PLACEMENT_3D('',#4215,#3425,#3426);
#2898=AXIS2_PLACEMENT_3D('',#4218,#3429,#3430);
#2899=AXIS2_PLACEMENT_3D('',#4219,#3431,#3432);
#2900=AXIS2_PLACEMENT_3D('',#4220,#3433,#3434);
#2901=AXIS2_PLACEMENT_3D('',#4222,#3435,#3436);
#2902=AXIS2_PLACEMENT_3D('',#4223,#3437,#3438);
#2903=AXIS2_PLACEMENT_3D('',#4225,#3439,#3440);
#2904=AXIS2_PLACEMENT_3D('',#4226,#3441,#3442);
#2905=AXIS2_PLACEMENT_3D('',#4228,#3443,#3444);
#2906=AXIS2_PLACEMENT_3D('',#4230,#3446,#3447);
#2907=AXIS2_PLACEMENT_3D('',#4232,#3448,#3449);
#2908=AXIS2_PLACEMENT_3D('',#4234,#3451,#3452);
#2909=AXIS2_PLACEMENT_3D('',#4236,#3453,#3454);
#2910=AXIS2_PLACEMENT_3D('',#4238,#3456,#3457);
#2911=AXIS2_PLACEMENT_3D('',#4240,#3458,#3459);
#2912=AXIS2_PLACEMENT_3D('',#4241,#3460,#3461);
#2913=AXIS2_PLACEMENT_3D('',#4243,#3462,#3463);
#2914=AXIS2_PLACEMENT_3D('',#4245,#3465,#3466);
#3397=DIRECTION('axis',(0.,0.,1.));
#3398=DIRECTION('refdir',(1.,0.,0.));
#3399=DIRECTION('center_axis',(0.866025403784439,0.,-0.5));
#3400=DIRECTION('ref_axis',(0.5,0.,0.866025403784439));
#3401=DIRECTION('',(-0.5,0.,-0.866025403784439));
#3402=DIRECTION('',(0.,-1.,0.));
#3403=DIRECTION('',(0.5,0.,0.866025403784439));
#3404=DIRECTION('',(0.,-1.,0.));
#3405=DIRECTION('center_axis',(1.20185167898973E-16,0.,-1.));
#3406=DIRECTION('ref_axis',(1.,0.,1.20185167898973E-16));
#3407=DIRECTION('',(-1.,0.,-1.20185167898973E-16));
#3408=DIRECTION('',(0.,-1.,0.));
#3409=DIRECTION('',(1.,0.,1.20185167898973E-16));
#3410=DIRECTION('center_axis',(-0.866025403784439,0.,-0.5));
#3411=DIRECTION('ref_axis',(0.5,0.,-0.866025403784439));
#3412=DIRECTION('',(-0.5,0.,0.866025403784439));
#3413=DIRECTION('',(0.,-1.,0.));
#3414=DIRECTION('',(0.5,0.,-0.866025403784439));
#3415=DIRECTION('center_axis',(-0.866025403784439,0.,0.5));
#3416=DIRECTION('ref_axis',(-0.5,0.,-0.866025403784439));
#3417=DIRECTION('',(0.5,0.,0.866025403784439));
#3418=DIRECTION('',(0.,-1.,0.));
#3419=DIRECTION('',(-0.5,0.,-0.866025403784439));
#3420=DIRECTION('center_axis',(-2.40370335797945E-16,0.,1.));
#3421=DIRECTION('ref_axis',(-1.,0.,-2.40370335797945E-16));
#3422=DIRECTION('',(1.,0.,2.40370335797945E-16));
#3423=DIRECTION('',(0.,-1.,0.));
#3424=DIRECTION('',(-1.,0.,-2.40370335797945E-16));
#3425=DIRECTION('center_axis',(0.866025403784439,0.,0.5));
#3426=DIRECTION('ref_axis',(-0.5,0.,0.866025403784439));
#3427=DIRECTION('',(0.5,0.,-0.866025403784439));
#3428=DIRECTION('',(-0.5,0.,0.866025403784439));
#3429=DIRECTION('center_axis',(0.,1.,0.));
#3430=DIRECTION('ref_axis',(1.,0.,0.));
#3431=DIRECTION('center_axis',(0.,-1.,0.));
#3432=DIRECTION('ref_axis',(0.,0.,-1.));
#3433=DIRECTION('center_axis',(0.,1.,0.));
#3434=DIRECTION('ref_axis',(1.,0.,0.));
#3435=DIRECTION('center_axis',(0.,1.,0.));
#3436=DIRECTION('ref_axis',(1.,0.,0.));
#3437=DIRECTION('center_axis',(0.,1.,0.));
#3438=DIRECTION('ref_axis',(0.,0.,1.));
#3439=DIRECTION('center_axis',(0.,-1.,0.));
#3440=DIRECTION('ref_axis',(1.,0.,0.));
#3441=DIRECTION('center_axis',(0.,-1.,0.));
#3442=DIRECTION('ref_axis',(1.,0.,0.));
#3443=DIRECTION('center_axis',(0.,-1.,0.));
#3444=DIRECTION('ref_axis',(1.,0.,0.));
#3445=DIRECTION('',(0.707106781186548,0.707106781186547,8.65956056235493E-17));
#3446=DIRECTION('center_axis',(0.,-1.,0.));
#3447=DIRECTION('ref_axis',(1.,0.,0.));
#3448=DIRECTION('center_axis',(0.,-1.,0.));
#3449=DIRECTION('ref_axis',(1.,0.,0.));
#3450=DIRECTION('',(0.,1.,0.));
#3451=DIRECTION('center_axis',(0.,1.,0.));
#3452=DIRECTION('ref_axis',(1.,0.,0.));
#3453=DIRECTION('center_axis',(0.,-1.,0.));
#3454=DIRECTION('ref_axis',(1.,0.,0.));
#3455=DIRECTION('',(-0.707106781186547,0.707106781186548,-8.65956056235493E-17));
#3456=DIRECTION('center_axis',(0.,-1.,0.));
#3457=DIRECTION('ref_axis',(0.,0.,-1.));
#3458=DIRECTION('center_axis',(0.,-1.,0.));
#3459=DIRECTION('ref_axis',(1.,0.,0.));
#3460=DIRECTION('center_axis',(0.,1.,0.));
#3461=DIRECTION('ref_axis',(1.,0.,0.));
#3462=DIRECTION('center_axis',(0.,1.,0.));
#3463=DIRECTION('ref_axis',(1.,0.,0.));
#3464=DIRECTION('',(-0.447213595499958,0.894427190999916,-5.47678698264203E-17));
#3465=DIRECTION('center_axis',(0.,-1.,0.));
#3466=DIRECTION('ref_axis',(1.,0.,0.));
#3467=DIRECTION('',(0.,1.,0.));
#4181=CARTESIAN_POINT('',(0.,0.,0.));
#4182=CARTESIAN_POINT('Origin',(0.115470053837925,-0.5,-0.2));
#4183=CARTESIAN_POINT('',(0.23094010767585,-0.5,0.));
#4184=CARTESIAN_POINT('',(0.115470053837925,-0.5,-0.2));
#4185=CARTESIAN_POINT('',(0.23094010767585,-0.5,0.));
#4186=CARTESIAN_POINT('',(0.115470053837925,-0.8,-0.2));
#4187=CARTESIAN_POINT('',(0.115470053837925,-0.5,-0.2));
#4188=CARTESIAN_POINT('',(0.23094010767585,-0.8,0.));
#4189=CARTESIAN_POINT('',(0.23094010767585,-0.8,0.));
#4190=CARTESIAN_POINT('',(0.23094010767585,-0.5,0.));
#4191=CARTESIAN_POINT('Origin',(-0.115470053837925,-0.5,-0.2));
#4192=CARTESIAN_POINT('',(-0.115470053837925,-0.5,-0.2));
#4193=CARTESIAN_POINT('',(0.115470053837925,-0.5,-0.2));
#4194=CARTESIAN_POINT('',(-0.115470053837925,-0.8,-0.2));
#4195=CARTESIAN_POINT('',(-0.115470053837925,-0.5,-0.2));
#4196=CARTESIAN_POINT('',(0.115470053837925,-0.8,-0.2));
#4197=CARTESIAN_POINT('Origin',(-0.23094010767585,-0.5,-2.77555756156289E-17));
#4198=CARTESIAN_POINT('',(-0.23094010767585,-0.5,-2.82820063659975E-17));
#4199=CARTESIAN_POINT('',(-0.115470053837925,-0.5,-0.2));
#4200=CARTESIAN_POINT('',(-0.23094010767585,-0.8,-2.77555756156289E-17));
#4201=CARTESIAN_POINT('',(-0.23094010767585,-0.5,-2.82820063659975E-17));
#4202=CARTESIAN_POINT('',(-0.115470053837925,-0.8,-0.2));
#4203=CARTESIAN_POINT('Origin',(-0.115470053837925,-0.5,0.2));
#4204=CARTESIAN_POINT('',(-0.115470053837925,-0.5,0.2));
#4205=CARTESIAN_POINT('',(-0.23094010767585,-0.5,-2.82820063659975E-17));
#4206=CARTESIAN_POINT('',(-0.115470053837925,-0.8,0.2));
#4207=CARTESIAN_POINT('',(-0.115470053837925,-0.5,0.2));
#4208=CARTESIAN_POINT('',(-0.23094010767585,-0.8,-2.82820063659975E-17));
#4209=CARTESIAN_POINT('Origin',(0.115470053837925,-0.5,0.2));
#4210=CARTESIAN_POINT('',(0.115470053837925,-0.5,0.2));
#4211=CARTESIAN_POINT('',(-0.115470053837925,-0.5,0.2));
#4212=CARTESIAN_POINT('',(0.115470053837925,-0.8,0.2));
#4213=CARTESIAN_POINT('',(0.115470053837925,-0.5,0.2));
#4214=CARTESIAN_POINT('',(-0.115470053837925,-0.8,0.2));
#4215=CARTESIAN_POINT('Origin',(0.23094010767585,-0.5,0.));
#4216=CARTESIAN_POINT('',(0.115470053837925,-0.5,0.2));
#4217=CARTESIAN_POINT('',(0.115470053837925,-0.8,0.2));
#4218=CARTESIAN_POINT('Origin',(0.,-0.5,0.));
#4219=CARTESIAN_POINT('Origin',(0.,-0.8,0.));
#4220=CARTESIAN_POINT('Origin',(0.,-1.4,0.));
#4221=CARTESIAN_POINT('',(-0.24505,-1.4,3.00099698131059E-17));
#4222=CARTESIAN_POINT('Origin',(0.,-1.4,0.));
#4223=CARTESIAN_POINT('Origin',(0.375,0.5,0.));
#4224=CARTESIAN_POINT('',(-0.375,0.5,-4.59242549680257E-17));
#4225=CARTESIAN_POINT('Origin',(0.,0.5,0.));
#4226=CARTESIAN_POINT('Origin',(0.,0.475,0.));
#4227=CARTESIAN_POINT('',(-0.425,0.45,-5.20474889637625E-17));
#4228=CARTESIAN_POINT('Origin',(0.,0.45,0.));
#4229=CARTESIAN_POINT('',(-0.4,0.475,-4.89858719658941E-17));
#4230=CARTESIAN_POINT('Origin',(0.,0.24,0.));
#4231=CARTESIAN_POINT('',(-0.425,0.0299999999999998,-5.20474889637625E-17));
#4232=CARTESIAN_POINT('Origin',(0.,0.0299999999999998,0.));
#4233=CARTESIAN_POINT('',(-0.425,0.24,-5.20474889637625E-17));
#4234=CARTESIAN_POINT('Origin',(0.,0.0150000000000001,0.));
#4235=CARTESIAN_POINT('',(-0.395,4.85722573273506E-17,-4.83735485663204E-17));
#4236=CARTESIAN_POINT('Origin',(0.,0.,0.));
#4237=CARTESIAN_POINT('',(-0.41,0.0150000000000001,-5.02105187650415E-17));
#4238=CARTESIAN_POINT('Origin',(0.27,0.,0.));
#4239=CARTESIAN_POINT('',(-0.27,0.,-3.30654635769785E-17));
#4240=CARTESIAN_POINT('Origin',(0.,0.,0.));
#4241=CARTESIAN_POINT('Origin',(0.,-0.02,0.));
#4242=CARTESIAN_POINT('',(-0.24505,-0.0498999999999999,3.00099698131059E-17));
#4243=CARTESIAN_POINT('Origin',(0.,-0.0498999999999999,0.));
#4244=CARTESIAN_POINT('',(-0.26,-0.02,-3.18408167778312E-17));
#4245=CARTESIAN_POINT('Origin',(0.,-0.995,0.));
#4246=CARTESIAN_POINT('',(-0.24505,-0.995,-3.00099698131059E-17));
#4760=UNCERTAINTY_MEASURE_WITH_UNIT(LENGTH_MEASURE(0.001),#4792,
'DISTANCE_ACCURACY_VALUE',
'Maximum model space distance between geometric entities at asserted c
onnectivities');
#4772=UNCERTAINTY_MEASURE_WITH_UNIT(LENGTH_MEASURE(0.001),#4792,
'DISTANCE_ACCURACY_VALUE',
'Maximum model space distance between geometric entities at asserted c
onnectivities');
#4779=(
GEOMETRIC_REPRESENTATION_CONTEXT(3)
GLOBAL_UNCERTAINTY_ASSIGNED_CONTEXT((#4760))
GLOBAL_UNIT_ASSIGNED_CONTEXT((#4792,#4794,#4795))
REPRESENTATION_CONTEXT('','3D')
);
#4791=(
GEOMETRIC_REPRESENTATION_CONTEXT(3)
GLOBAL_UNCERTAINTY_ASSIGNED_CONTEXT((#4772))
GLOBAL_UNIT_ASSIGNED_CONTEXT((#4792,#4794,#4795))
REPRESENTATION_CONTEXT('','3D')
);
#4792=(
LENGTH_UNIT()
NAMED_UNIT(*)
SI_UNIT(.CENTI.,.METRE.)
);
#4794=(
NAMED_UNIT(*)
PLANE_ANGLE_UNIT()
SI_UNIT($,.RADIAN.)
);
#4795=(
NAMED_UNIT(*)
SI_UNIT($,.STERADIAN.)
SOLID_ANGLE_UNIT()
);
#4802=SHAPE_DEFINITION_REPRESENTATION(#4820,#4866);
#4820=PRODUCT_DEFINITION_SHAPE('',$,#4885);
#4866=SHAPE_REPRESENTATION('',(#2891),#4779);
#4878=PRODUCT_DEFINITION_CONTEXT('part definition',#4934,'design');
#4885=PRODUCT_DEFINITION('M5x14 Cap Screw','M5x14 Cap Screw',#4903,#4878);
#4903=PRODUCT_DEFINITION_FORMATION('',$,#4942);
#4934=APPLICATION_CONTEXT(
'Core Data for Automotive Mechanical Design Process');
#4935=PRODUCT_CONTEXT('part definition',#4934,'mechanical');
#4942=PRODUCT('M5x14 Cap Screw','M5x14 Cap Screw','M5x14 Cap Screw',(#4935));
#5024=COLOUR_RGB('Black',0.12,0.14,0.17);
#5025=FILL_AREA_STYLE_COLOUR('',#5024);
#5026=FILL_AREA_STYLE('',(#5025));
#5027=SURFACE_STYLE_FILL_AREA(#5026);
#5028=SURFACE_SIDE_STYLE('',(#5027));
#5029=SURFACE_STYLE_USAGE(.BOTH.,#5028);
#5030=PRESENTATION_STYLE_ASSIGNMENT((#5029));
ENDSEC;
END-ISO-10303-21;
